ISO-10303-21;
HEADER;
/* Generated by software containing ST-Developer
 * from STEP Tools, Inc. (www.steptools.com) 
 */

FILE_DESCRIPTION(
/* description */ ('Caster wheel assembly'),
/* implementation_level */ '2;1');

FILE_NAME(
/* name */ 'Hex Nut - M8.step',
/* time_stamp */ '2026-10-28T03:23:56-07:00',
/* author */ (''),
/* organization */ (''),
/* preprocessor_version */ 'ST-DEVELOPER v20.2',
/* originating_system */ 'Autodesk Translation Framework v15.17.0.0',
/* authorisation */ '');

FILE_SCHEMA (('AUTOMOTIVE_DESIGN { 1 0 10303 214 3 1 1 }'));
ENDSEC;

DATA;
#10=MECHANICAL_DESIGN_GEOMETRIC_PRESENTATION_REPRESENTATION('',(#226),#5385);
#157=(
BOUNDED_CURVE()
B_SPLINE_CURVE(2,(#4316,#4317,#4318),.UNSPECIFIED.,.F.,.F.)
B_SPLINE_CURVE_WITH_KNOTS((3,3),(0.14973948338295,0.97160236658079),
 .UNSPECIFIED.)
CURVE()
GEOMETRIC_REPRESENTATION_ITEM()
RATIONAL_B_SPLINE_CURVE((1.07140024848292,1.23714644374248,1.07140024848292))
REPRESENTATION_ITEM('')
);
#158=(
BOUNDED_CURVE()
B_SPLINE_CURVE(2,(#4320,#4321,#4322),.UNSPECIFIED.,.F.,.F.)
B_SPLINE_CURVE_WITH_KNOTS((3,3),(0.14973948338295,0.971602366580789),
 .UNSPECIFIED.)
CURVE()
GEOMETRIC_REPRESENTATION_ITEM()
RATIONAL_B_SPLINE_CURVE((1.07140024848292,1.23714644374248,1.07140024848292))
REPRESENTATION_ITEM('')
);
#159=(
BOUNDED_CURVE()
B_SPLINE_CURVE(2,(#4327,#4328,#4329),.UNSPECIFIED.,.F.,.F.)
B_SPLINE_CURVE_WITH_KNOTS((3,3),(0.14973948338295,0.97160236658079),
 .UNSPECIFIED.)
CURVE()
GEOMETRIC_REPRESENTATION_ITEM()
RATIONAL_B_SPLINE_CURVE((1.07140024848292,1.23714644374248,1.07140024848292))
REPRESENTATION_ITEM('')
);
#160=(
BOUNDED_CURVE()
B_SPLINE_CURVE(2,(#4331,#4332,#4333),.UNSPECIFIED.,.F.,.F.)
B_SPLINE_CURVE_WITH_KNOTS((3,3),(0.14973948338295,0.97160236658079),
 .UNSPECIFIED.)
CURVE()
GEOMETRIC_REPRESENTATION_ITEM()
RATIONAL_B_SPLINE_CURVE((1.07140024848292,1.23714644374248,1.07140024848292))
REPRESENTATION_ITEM('')
);
#161=(
BOUNDED_CURVE()
B_SPLINE_CURVE(2,(#4335,#4336,#4337),.UNSPECIFIED.,.F.,.F.)
B_SPLINE_CURVE_WITH_KNOTS((3,3),(0.14973948338295,0.971602366580789),
 .UNSPECIFIED.)
CURVE()
GEOMETRIC_REPRESENTATION_ITEM()
RATIONAL_B_SPLINE_CURVE((1.07140024848292,1.23714644374248,1.07140024848292))
REPRESENTATION_ITEM('')
);
#162=(
BOUNDED_CURVE()
B_SPLINE_CURVE(2,(#4338,#4339,#4340),.UNSPECIFIED.,.F.,.F.)
B_SPLINE_CURVE_WITH_KNOTS((3,3),(0.14973948338295,0.97160236658079),
 .UNSPECIFIED.)
CURVE()
GEOMETRIC_REPRESENTATION_ITEM()
RATIONAL_B_SPLINE_CURVE((1.07140024848292,1.23714644374248,1.07140024848292))
REPRESENTATION_ITEM('')
);
#163=(
BOUNDED_CURVE()
B_SPLINE_CURVE(2,(#4347,#4348,#4349),.UNSPECIFIED.,.F.,.F.)
B_SPLINE_CURVE_WITH_KNOTS((3,3),(0.14973948338295,0.97160236658079),
 .UNSPECIFIED.)
CURVE()
GEOMETRIC_REPRESENTATION_ITEM()
RATIONAL_B_SPLINE_CURVE((1.07140024848292,1.23714644374248,1.07140024848292))
REPRESENTATION_ITEM('')
);
#164=(
BOUNDED_CURVE()
B_SPLINE_CURVE(2,(#4351,#4352,#4353),.UNSPECIFIED.,.F.,.F.)
B_SPLINE_CURVE_WITH_KNOTS((3,3),(0.14973948338295,0.97160236658079),
 .UNSPECIFIED.)
CURVE()
GEOMETRIC_REPRESENTATION_ITEM()
RATIONAL_B_SPLINE_CURVE((1.07140024848292,1.23714644374248,1.07140024848292))
REPRESENTATION_ITEM('')
);
#165=(
BOUNDED_CURVE()
B_SPLINE_CURVE(2,(#4355,#4356,#4357),.UNSPECIFIED.,.F.,.F.)
B_SPLINE_CURVE_WITH_KNOTS((3,3),(0.14973948338295,0.971602366580789),
 .UNSPECIFIED.)
CURVE()
GEOMETRIC_REPRESENTATION_ITEM()
RATIONAL_B_SPLINE_CURVE((1.07140024848292,1.23714644374248,1.07140024848292))
REPRESENTATION_ITEM('')
);
#166=(
BOUNDED_CURVE()
B_SPLINE_CURVE(2,(#4359,#4360,#4361),.UNSPECIFIED.,.F.,.F.)
B_SPLINE_CURVE_WITH_KNOTS((3,3),(0.14973948338295,0.97160236658079),
 .UNSPECIFIED.)
CURVE()
GEOMETRIC_REPRESENTATION_ITEM()
RATIONAL_B_SPLINE_CURVE((1.07140024848292,1.23714644374248,1.07140024848292))
REPRESENTATION_ITEM('')
);
#167=(
BOUNDED_CURVE()
B_SPLINE_CURVE(2,(#4363,#4364,#4365),.UNSPECIFIED.,.F.,.F.)
B_SPLINE_CURVE_WITH_KNOTS((3,3),(0.14973948338295,0.97160236658079),
 .UNSPECIFIED.)
CURVE()
GEOMETRIC_REPRESENTATION_ITEM()
RATIONAL_B_SPLINE_CURVE((1.07140024848292,1.23714644374248,1.07140024848292))
REPRESENTATION_ITEM('')
);
#168=(
BOUNDED_CURVE()
B_SPLINE_CURVE(2,(#4366,#4367,#4368),.UNSPECIFIED.,.F.,.F.)
B_SPLINE_CURVE_WITH_KNOTS((3,3),(0.14973948338295,0.971602366580789),
 .UNSPECIFIED.)
CURVE()
GEOMETRIC_REPRESENTATION_ITEM()
RATIONAL_B_SPLINE_CURVE((1.07140024848292,1.23714644374248,1.07140024848292))
REPRESENTATION_ITEM('')
);
#169=CONICAL_SURFACE('',#2980,0.734027674973257,1.0471975511966);
#170=CONICAL_SURFACE('',#2982,0.734027674973257,1.0471975511966);
#182=SHAPE_REPRESENTATION_RELATIONSHIP('SRR','None',#5477,#204);
#204=ADVANCED_BREP_SHAPE_REPRESENTATION('',(#256),#5364);
#226=STYLED_ITEM('',(#5679),#256);
#256=MANIFOLD_SOLID_BREP('Body1',#2653);
#297=FACE_BOUND('',#641,.T.);
#298=FACE_BOUND('',#643,.T.);
#347=PLANE('',#2984);
#348=PLANE('',#2985);
#349=PLANE('',#2986);
#350=PLANE('',#2990);
#351=PLANE('',#2991);
#352=PLANE('',#2992);
#353=PLANE('',#2993);
#354=PLANE('',#2994);
#447=FACE_OUTER_BOUND('',#631,.T.);
#448=FACE_OUTER_BOUND('',#632,.T.);
#449=FACE_OUTER_BOUND('',#633,.T.);
#450=FACE_OUTER_BOUND('',#634,.T.);
#451=FACE_OUTER_BOUND('',#635,.T.);
#452=FACE_OUTER_BOUND('',#636,.T.);
#453=FACE_OUTER_BOUND('',#637,.T.);
#454=FACE_OUTER_BOUND('',#638,.T.);
#455=FACE_OUTER_BOUND('',#639,.T.);
#456=FACE_OUTER_BOUND('',#640,.T.);
#457=FACE_OUTER_BOUND('',#642,.T.);
#631=EDGE_LOOP('',(#1878,#1879,#1880,#1881,#1882,#1883,#1884,#1885,#1886));
#632=EDGE_LOOP('',(#1887,#1888,#1889,#1890,#1891,#1892,#1893,#1894,#1895));
#633=EDGE_LOOP('',(#1896,#1897,#1898,#1899));
#634=EDGE_LOOP('',(#1900,#1901,#1902,#1903));
#635=EDGE_LOOP('',(#1904,#1905,#1906,#1907));
#636=EDGE_LOOP('',(#1908,#1909,#1910,#1911));
#637=EDGE_LOOP('',(#1912,#1913,#1914,#1915));
#638=EDGE_LOOP('',(#1916,#1917,#1918,#1919));
#639=EDGE_LOOP('',(#1920,#1921,#1922,#1923));
#640=EDGE_LOOP('',(#1924));
#641=EDGE_LOOP('',(#1925));
#642=EDGE_LOOP('',(#1926));
#643=EDGE_LOOP('',(#1927));
#833=LINE('',#4324,#967);
#834=LINE('',#4345,#968);
#835=LINE('',#4370,#969);
#836=LINE('',#4371,#970);
#837=LINE('',#4373,#971);
#838=LINE('',#4375,#972);
#839=LINE('',#4380,#973);
#840=LINE('',#4383,#974);
#841=LINE('',#4385,#975);
#967=VECTOR('',#3444,0.734027674973257);
#968=VECTOR('',#3451,0.734027674973257);
#969=VECTOR('',#3454,1.);
#970=VECTOR('',#3455,1.);
#971=VECTOR('',#3458,1.);
#972=VECTOR('',#3461,1.);
#973=VECTOR('',#3466,0.4);
#974=VECTOR('',#3471,1.);
#975=VECTOR('',#3474,1.);
#1101=CIRCLE('',#2981,0.6175);
#1102=CIRCLE('',#2983,0.6175);
#1103=CIRCLE('',#2988,0.338975);
#1104=CIRCLE('',#2989,0.338975);
#1268=VERTEX_POINT('',#4314);
#1269=VERTEX_POINT('',#4315);
#1270=VERTEX_POINT('',#4319);
#1271=VERTEX_POINT('',#4323);
#1272=VERTEX_POINT('',#4326);
#1273=VERTEX_POINT('',#4330);
#1274=VERTEX_POINT('',#4334);
#1275=VERTEX_POINT('',#4342);
#1276=VERTEX_POINT('',#4344);
#1277=VERTEX_POINT('',#4346);
#1278=VERTEX_POINT('',#4350);
#1279=VERTEX_POINT('',#4354);
#1280=VERTEX_POINT('',#4358);
#1281=VERTEX_POINT('',#4362);
#1282=VERTEX_POINT('',#4377);
#1283=VERTEX_POINT('',#4379);
#1507=EDGE_CURVE('',#1268,#1269,#157,.T.);
#1508=EDGE_CURVE('',#1270,#1268,#158,.T.);
#1509=EDGE_CURVE('',#1270,#1271,#833,.T.);
#1510=EDGE_CURVE('',#1271,#1271,#1101,.T.);
#1511=EDGE_CURVE('',#1272,#1270,#159,.T.);
#1512=EDGE_CURVE('',#1273,#1272,#160,.T.);
#1513=EDGE_CURVE('',#1274,#1273,#161,.T.);
#1514=EDGE_CURVE('',#1269,#1274,#162,.T.);
#1515=EDGE_CURVE('',#1275,#1275,#1102,.T.);
#1516=EDGE_CURVE('',#1275,#1276,#834,.T.);
#1517=EDGE_CURVE('',#1277,#1276,#163,.T.);
#1518=EDGE_CURVE('',#1278,#1277,#164,.T.);
#1519=EDGE_CURVE('',#1279,#1278,#165,.T.);
#1520=EDGE_CURVE('',#1280,#1279,#166,.T.);
#1521=EDGE_CURVE('',#1281,#1280,#167,.T.);
#1522=EDGE_CURVE('',#1276,#1281,#168,.T.);
#1523=EDGE_CURVE('',#1272,#1281,#835,.T.);
#1524=EDGE_CURVE('',#1273,#1280,#836,.T.);
#1525=EDGE_CURVE('',#1270,#1276,#837,.T.);
#1526=EDGE_CURVE('',#1268,#1277,#838,.T.);
#1527=EDGE_CURVE('',#1282,#1282,#1103,.F.);
#1528=EDGE_CURVE('',#1282,#1283,#839,.T.);
#1529=EDGE_CURVE('',#1283,#1283,#1104,.F.);
#1530=EDGE_CURVE('',#1269,#1278,#840,.T.);
#1531=EDGE_CURVE('',#1274,#1279,#841,.T.);
#1878=ORIENTED_EDGE('',*,*,#1507,.F.);
#1879=ORIENTED_EDGE('',*,*,#1508,.F.);
#1880=ORIENTED_EDGE('',*,*,#1509,.T.);
#1881=ORIENTED_EDGE('',*,*,#1510,.F.);
#1882=ORIENTED_EDGE('',*,*,#1509,.F.);
#1883=ORIENTED_EDGE('',*,*,#1511,.F.);
#1884=ORIENTED_EDGE('',*,*,#1512,.F.);
#1885=ORIENTED_EDGE('',*,*,#1513,.F.);
#1886=ORIENTED_EDGE('',*,*,#1514,.F.);
#1887=ORIENTED_EDGE('',*,*,#1515,.F.);
#1888=ORIENTED_EDGE('',*,*,#1516,.T.);
#1889=ORIENTED_EDGE('',*,*,#1517,.F.);
#1890=ORIENTED_EDGE('',*,*,#1518,.F.);
#1891=ORIENTED_EDGE('',*,*,#1519,.F.);
#1892=ORIENTED_EDGE('',*,*,#1520,.F.);
#1893=ORIENTED_EDGE('',*,*,#1521,.F.);
#1894=ORIENTED_EDGE('',*,*,#1522,.F.);
#1895=ORIENTED_EDGE('',*,*,#1516,.F.);
#1896=ORIENTED_EDGE('',*,*,#1512,.T.);
#1897=ORIENTED_EDGE('',*,*,#1523,.T.);
#1898=ORIENTED_EDGE('',*,*,#1521,.T.);
#1899=ORIENTED_EDGE('',*,*,#1524,.F.);
#1900=ORIENTED_EDGE('',*,*,#1511,.T.);
#1901=ORIENTED_EDGE('',*,*,#1525,.T.);
#1902=ORIENTED_EDGE('',*,*,#1522,.T.);
#1903=ORIENTED_EDGE('',*,*,#1523,.F.);
#1904=ORIENTED_EDGE('',*,*,#1508,.T.);
#1905=ORIENTED_EDGE('',*,*,#1526,.T.);
#1906=ORIENTED_EDGE('',*,*,#1517,.T.);
#1907=ORIENTED_EDGE('',*,*,#1525,.F.);
#1908=ORIENTED_EDGE('',*,*,#1527,.F.);
#1909=ORIENTED_EDGE('',*,*,#1528,.T.);
#1910=ORIENTED_EDGE('',*,*,#1529,.T.);
#1911=ORIENTED_EDGE('',*,*,#1528,.F.);
#1912=ORIENTED_EDGE('',*,*,#1507,.T.);
#1913=ORIENTED_EDGE('',*,*,#1530,.T.);
#1914=ORIENTED_EDGE('',*,*,#1518,.T.);
#1915=ORIENTED_EDGE('',*,*,#1526,.F.);
#1916=ORIENTED_EDGE('',*,*,#1513,.T.);
#1917=ORIENTED_EDGE('',*,*,#1524,.T.);
#1918=ORIENTED_EDGE('',*,*,#1520,.T.);
#1919=ORIENTED_EDGE('',*,*,#1531,.F.);
#1920=ORIENTED_EDGE('',*,*,#1514,.T.);
#1921=ORIENTED_EDGE('',*,*,#1531,.T.);
#1922=ORIENTED_EDGE('',*,*,#1519,.T.);
#1923=ORIENTED_EDGE('',*,*,#1530,.F.);
#1924=ORIENTED_EDGE('',*,*,#1515,.T.);
#1925=ORIENTED_EDGE('',*,*,#1527,.T.);
#1926=ORIENTED_EDGE('',*,*,#1510,.T.);
#1927=ORIENTED_EDGE('',*,*,#1529,.F.);
#2440=CYLINDRICAL_SURFACE('',#2987,0.338975);
#2507=ADVANCED_FACE('',(#447),#169,.T.);
#2508=ADVANCED_FACE('',(#448),#170,.T.);
#2509=ADVANCED_FACE('',(#449),#347,.T.);
#2510=ADVANCED_FACE('',(#450),#348,.T.);
#2511=ADVANCED_FACE('',(#451),#349,.T.);
#2512=ADVANCED_FACE('',(#452),#2440,.F.);
#2513=ADVANCED_FACE('',(#453),#350,.T.);
#2514=ADVANCED_FACE('',(#454),#351,.T.);
#2515=ADVANCED_FACE('',(#455),#352,.T.);
#2516=ADVANCED_FACE('',(#456,#297),#353,.T.);
#2517=ADVANCED_FACE('',(#457,#298),#354,.F.);
#2653=CLOSED_SHELL('',(#2507,#2508,#2509,#2510,#2511,#2512,#2513,#2514,
#2515,#2516,#2517));
#2979=AXIS2_PLACEMENT_3D('',#4312,#3440,#3441);
#2980=AXIS2_PLACEMENT_3D('',#4313,#3442,#3443);
#2981=AXIS2_PLACEMENT_3D('',#4325,#3445,#3446);
#2982=AXIS2_PLACEMENT_3D('',#4341,#3447,#3448);
#2983=AXIS2_PLACEMENT_3D('',#4343,#3449,#3450);
#2984=AXIS2_PLACEMENT_3D('',#4369,#3452,#3453);
#2985=AXIS2_PLACEMENT_3D('',#4372,#3456,#3457);
#2986=AXIS2_PLACEMENT_3D('',#4374,#3459,#3460);
#2987=AXIS2_PLACEMENT_3D('',#4376,#3462,#3463);
#2988=AXIS2_PLACEMENT_3D('',#4378,#3464,#3465);
#2989=AXIS2_PLACEMENT_3D('',#4381,#3467,#3468);
#2990=AXIS2_PLACEMENT_3D('',#4382,#3469,#3470);
#2991=AXIS2_PLACEMENT_3D('',#4384,#3472,#3473);
#2992=AXIS2_PLACEMENT_3D('',#4386,#3475,#3476);
#2993=AXIS2_PLACEMENT_3D('',#4387,#3477,#3478);
#2994=AXIS2_PLACEMENT_3D('',#4388,#3479,#3480);
#3440=DIRECTION('axis',(0.,0.,1.));
#3441=DIRECTION('refdir',(1.,0.,0.));
#3442=DIRECTION('center_axis',(0.,1.,0.));
#3443=DIRECTION('ref_axis',(1.,0.,0.));
#3444=DIRECTION('',(0.866025403784439,-0.5,1.06057523872491E-16));
#3445=DIRECTION('center_axis',(0.,-1.,0.));
#3446=DIRECTION('ref_axis',(1.,0.,0.));
#3447=DIRECTION('center_axis',(0.,-1.,0.));
#3448=DIRECTION('ref_axis',(1.,0.,0.));
#3449=DIRECTION('center_axis',(0.,1.,0.));
#3450=DIRECTION('ref_axis',(1.,0.,0.));
#3451=DIRECTION('',(-0.866025403784439,-0.5,-1.06057523872491E-16));
#3452=DIRECTION('center_axis',(1.4792020664489E-16,0.,-1.));
#3453=DIRECTION('ref_axis',(-1.,0.,-1.4792020664489E-16));
#3454=DIRECTION('',(0.,1.,0.));
#3455=DIRECTION('',(0.,1.,0.));
#3456=DIRECTION('center_axis',(-0.866025403784439,0.,-0.5));
#3457=DIRECTION('ref_axis',(-0.5,0.,0.866025403784439));
#3458=DIRECTION('',(0.,1.,0.));
#3459=DIRECTION('center_axis',(-0.866025403784439,0.,0.5));
#3460=DIRECTION('ref_axis',(0.5,0.,0.866025403784439));
#3461=DIRECTION('',(0.,1.,0.));
#3462=DIRECTION('center_axis',(0.,1.,0.));
#3463=DIRECTION('ref_axis',(1.,0.,0.));
#3464=DIRECTION('center_axis',(0.,1.,0.));
#3465=DIRECTION('ref_axis',(1.,0.,0.));
#3466=DIRECTION('',(0.,-1.,0.));
#3467=DIRECTION('center_axis',(0.,1.,0.));
#3468=DIRECTION('ref_axis',(1.,0.,0.));
#3469=DIRECTION('center_axis',(-2.95840413289779E-16,0.,1.));
#3470=DIRECTION('ref_axis',(1.,0.,2.95840413289779E-16));
#3471=DIRECTION('',(0.,1.,0.));
#3472=DIRECTION('center_axis',(0.866025403784439,0.,-0.5));
#3473=DIRECTION('ref_axis',(-0.5,0.,-0.866025403784439));
#3474=DIRECTION('',(0.,1.,0.));
#3475=DIRECTION('center_axis',(0.866025403784439,0.,0.5));
#3476=DIRECTION('ref_axis',(0.5,0.,-0.866025403784439));
#3477=DIRECTION('center_axis',(0.,1.,0.));
#3478=DIRECTION('ref_axis',(1.,0.,0.));
#3479=DIRECTION('center_axis',(0.,1.,0.));
#3480=DIRECTION('ref_axis',(1.,0.,0.));
#4312=CARTESIAN_POINT('',(0.,0.,0.));
#4313=CARTESIAN_POINT('Origin',(0.,0.067277284513851,0.));
#4314=CARTESIAN_POINT('',(-0.375277674973257,0.0768195421087395,0.65));
#4315=CARTESIAN_POINT('',(0.375277674973257,0.0768195421087395,0.65));
#4316=CARTESIAN_POINT('Ctrl Pts',(-0.375277674973257,0.0768195421087395,
0.65));
#4317=CARTESIAN_POINT('Ctrl Pts',(1.66533453693773E-13,-0.0315137912242439,
0.65));
#4318=CARTESIAN_POINT('Ctrl Pts',(0.375277674973257,0.0768195421087394,
0.65));
#4319=CARTESIAN_POINT('',(-0.750555349946514,0.0768195421087394,-9.19165206894919E-17));
#4320=CARTESIAN_POINT('Ctrl Pts',(-0.750555349946514,0.0768195421087394,
-9.19165206894919E-17));
#4321=CARTESIAN_POINT('Ctrl Pts',(-0.562916512459802,-0.0315137912242434,
0.325000000000144));
#4322=CARTESIAN_POINT('Ctrl Pts',(-0.375277674973257,0.0768195421087395,
0.65));
#4323=CARTESIAN_POINT('',(-0.6175,-2.77555756156289E-17,-7.5621939847349E-17));
#4324=CARTESIAN_POINT('',(-0.734027674973257,0.067277284513851,-8.98924642641573E-17));
#4325=CARTESIAN_POINT('Origin',(0.,0.,0.));
#4326=CARTESIAN_POINT('',(-0.375277674973257,0.0768195421087395,-0.65));
#4327=CARTESIAN_POINT('Ctrl Pts',(-0.375277674973257,0.0768195421087395,
-0.65));
#4328=CARTESIAN_POINT('Ctrl Pts',(-0.562916512459968,-0.0315137912242437,
-0.324999999999856));
#4329=CARTESIAN_POINT('Ctrl Pts',(-0.750555349946514,0.0768195421087395,
-9.19165206894919E-17));
#4330=CARTESIAN_POINT('',(0.375277674973257,0.0768195421087395,-0.65));
#4331=CARTESIAN_POINT('Ctrl Pts',(0.375277674973257,0.0768195421087395,
-0.65));
#4332=CARTESIAN_POINT('Ctrl Pts',(-1.66144875635155E-13,-0.0315137912242437,
-0.65));
#4333=CARTESIAN_POINT('Ctrl Pts',(-0.375277674973257,0.0768195421087395,
-0.65));
#4334=CARTESIAN_POINT('',(0.750555349946514,0.0768195421087394,0.));
#4335=CARTESIAN_POINT('Ctrl Pts',(0.750555349946514,0.0768195421087394,
0.));
#4336=CARTESIAN_POINT('Ctrl Pts',(0.562916512459802,-0.0315137912242436,
-0.325000000000144));
#4337=CARTESIAN_POINT('Ctrl Pts',(0.375277674973257,0.0768195421087395,
-0.65));
#4338=CARTESIAN_POINT('Ctrl Pts',(0.375277674973257,0.0768195421087394,
0.65));
#4339=CARTESIAN_POINT('Ctrl Pts',(0.562916512459968,-0.0315137912242439,
0.324999999999856));
#4340=CARTESIAN_POINT('Ctrl Pts',(0.750555349946514,0.0768195421087394,
0.));
#4341=CARTESIAN_POINT('Origin',(0.,0.612722715486149,0.));
#4342=CARTESIAN_POINT('',(-0.6175,0.68,-7.5621939847349E-17));
#4343=CARTESIAN_POINT('Origin',(0.,0.68,0.));
#4344=CARTESIAN_POINT('',(-0.750555349946514,0.603180457891261,-9.19165206894919E-17));
#4345=CARTESIAN_POINT('',(-0.734027674973257,0.612722715486149,-8.98924642641573E-17));
#4346=CARTESIAN_POINT('',(-0.375277674973257,0.603180457891261,0.65));
#4347=CARTESIAN_POINT('Ctrl Pts',(-0.375277674973257,0.603180457891261,
0.65));
#4348=CARTESIAN_POINT('Ctrl Pts',(-0.562916512459968,0.711513791224243,
0.324999999999856));
#4349=CARTESIAN_POINT('Ctrl Pts',(-0.750555349946514,0.603180457891261,
-9.19165206894919E-17));
#4350=CARTESIAN_POINT('',(0.375277674973257,0.603180457891261,0.65));
#4351=CARTESIAN_POINT('Ctrl Pts',(0.375277674973257,0.603180457891261,0.65));
#4352=CARTESIAN_POINT('Ctrl Pts',(-1.66755498298699E-13,0.711513791224244,
0.65));
#4353=CARTESIAN_POINT('Ctrl Pts',(-0.375277674973257,0.603180457891261,
0.65));
#4354=CARTESIAN_POINT('',(0.750555349946514,0.603180457891261,0.));
#4355=CARTESIAN_POINT('Ctrl Pts',(0.750555349946514,0.603180457891261,0.));
#4356=CARTESIAN_POINT('Ctrl Pts',(0.562916512459802,0.711513791224244,0.325000000000144));
#4357=CARTESIAN_POINT('Ctrl Pts',(0.375277674973257,0.603180457891261,0.65));
#4358=CARTESIAN_POINT('',(0.375277674973257,0.603180457891261,-0.65));
#4359=CARTESIAN_POINT('Ctrl Pts',(0.375277674973257,0.603180457891261,-0.65));
#4360=CARTESIAN_POINT('Ctrl Pts',(0.562916512459969,0.711513791224244,-0.324999999999856));
#4361=CARTESIAN_POINT('Ctrl Pts',(0.750555349946514,0.603180457891261,0.));
#4362=CARTESIAN_POINT('',(-0.375277674973257,0.603180457891261,-0.65));
#4363=CARTESIAN_POINT('Ctrl Pts',(-0.375277674973257,0.603180457891261,
-0.65));
#4364=CARTESIAN_POINT('Ctrl Pts',(1.66422431391311E-13,0.711513791224244,
-0.65));
#4365=CARTESIAN_POINT('Ctrl Pts',(0.375277674973257,0.603180457891261,-0.65));
#4366=CARTESIAN_POINT('Ctrl Pts',(-0.750555349946514,0.603180457891261,
-9.19165206894919E-17));
#4367=CARTESIAN_POINT('Ctrl Pts',(-0.562916512459802,0.711513791224244,
-0.325000000000144));
#4368=CARTESIAN_POINT('Ctrl Pts',(-0.375277674973257,0.603180457891261,
-0.65));
#4369=CARTESIAN_POINT('Origin',(0.375277674973257,0.,-0.65));
#4370=CARTESIAN_POINT('',(-0.375277674973257,0.,-0.65));
#4371=CARTESIAN_POINT('',(0.375277674973257,0.,-0.65));
#4372=CARTESIAN_POINT('Origin',(-0.375277674973257,0.,-0.65));
#4373=CARTESIAN_POINT('',(-0.750555349946514,0.,-9.19165206894919E-17));
#4374=CARTESIAN_POINT('Origin',(-0.750555349946514,0.,-9.19165206894919E-17));
#4375=CARTESIAN_POINT('',(-0.375277674973257,0.,0.65));
#4376=CARTESIAN_POINT('Origin',(0.,0.,0.));
#4377=CARTESIAN_POINT('',(-0.338975,0.68,4.15124648740974E-17));
#4378=CARTESIAN_POINT('Origin',(0.,0.68,0.));
#4379=CARTESIAN_POINT('',(-0.338975,0.,4.15124648740974E-17));
#4380=CARTESIAN_POINT('',(-0.338975,0.,4.15124648740974E-17));
#4381=CARTESIAN_POINT('Origin',(0.,0.,0.));
#4382=CARTESIAN_POINT('Origin',(-0.375277674973257,0.,0.65));
#4383=CARTESIAN_POINT('',(0.375277674973257,0.,0.65));
#4384=CARTESIAN_POINT('Origin',(0.750555349946514,0.,0.));
#4385=CARTESIAN_POINT('',(0.750555349946514,0.,0.));
#4386=CARTESIAN_POINT('Origin',(0.375277674973257,0.,0.65));
#4387=CARTESIAN_POINT('Origin',(0.,0.68,-1.11022302462516E-16));
#4388=CARTESIAN_POINT('Origin',(0.,0.,-1.11022302462516E-16));
#5336=UNCERTAINTY_MEASURE_WITH_UNIT(LENGTH_MEASURE(0.001),#5386,
'DISTANCE_ACCURACY_VALUE',
'Maximum model space distance between geometric entities at asserted c
onnectivities');
#5357=UNCERTAINTY_MEASURE_WITH_UNIT(LENGTH_MEASURE(0.001),#5386,
'DISTANCE_ACCURACY_VALUE',
'Maximum model space distance between geometric entities at asserted c
onnectivities');
#5364=(
GEOMETRIC_REPRESENTATION_CONTEXT(3)
GLOBAL_UNCERTAINTY_ASSIGNED_CONTEXT((#5336))
GLOBAL_UNIT_ASSIGNED_CONTEXT((#5386,#5388,#5389))
REPRESENTATION_CONTEXT('','3D')
);
#5385=(
GEOMETRIC_REPRESENTATION_CONTEXT(3)
GLOBAL_UNCERTAINTY_ASSIGNED_CONTEXT((#5357))
GLOBAL_UNIT_ASSIGNED_CONTEXT((#5386,#5388,#5389))
REPRESENTATION_CONTEXT('','3D')
);
#5386=(
LENGTH_UNIT()
NAMED_UNIT(*)
SI_UNIT(.CENTI.,.METRE.)
);
#5388=(
NAMED_UNIT(*)
PLANE_ANGLE_UNIT()
SI_UNIT($,.RADIAN.)
);
#5389=(
NAMED_UNIT(*)
SI_UNIT($,.STERADIAN.)
SOLID_ANGLE_UNIT()
);
#5396=SHAPE_DEFINITION_REPRESENTATION(#5423,#5477);
#5423=PRODUCT_DEFINITION_SHAPE('',$,#5505);
#5477=SHAPE_REPRESENTATION('',(#2979),#5364);
#5498=PRODUCT_DEFINITION_CONTEXT('part definition',#5581,'design');
#5505=PRODUCT_DEFINITION('Hex Nut - M8','Hex Nut - M8',#5532,#5498);
#5532=PRODUCT_DEFINITION_FORMATION('',$,#5589);
#5581=APPLICATION_CONTEXT(
'Core Data for Automotive Mechanical Design Process');
#5582=PRODUCT_CONTEXT('part definition',#5581,'mechanical');
#5589=PRODUCT('Hex Nut - M8','Hex Nut - M8','Hex Nut - M8',(#5582));
#5673=COLOUR_RGB('Black',0.12,0.14,0.17);
#5674=FILL_AREA_STYLE_COLOUR('',#5673);
#5675=FILL_AREA_STYLE('',(#5674));
#5676=SURFACE_STYLE_FILL_AREA(#5675);
#5677=SURFACE_SIDE_STYLE('',(#5676));
#5678=SURFACE_STYLE_USAGE(.BOTH.,#5677);
#5679=PRESENTATION_STYLE_ASSIGNMENT((#5678));
ENDSEC;
END-ISO-10303-21;
